ISO-10303-21;
HEADER;
FILE_DESCRIPTION (('STEP AP214'),
    '1' );
FILE_NAME ('16. Bolt M6x25.step',
    '2026-10-09T08:13:37',
    ( '' ),
    ( '' ),
    'SwSTEP 2.0',
    'SolidWorks 2021',
    '' );
FILE_SCHEMA (( 'AUTOMOTIVE_DESIGN' ));
ENDSEC;

DATA;
#47=CARTESIAN_POINT ( 'NONE',  ( 5.000000000000000000, 6.123233995736766282E-16, 0.7500000000000000000 ) ) ;
#130=UNCERTAINTY_MEASURE_WITH_UNIT (LENGTH_MEASURE( 1.000000000000000082E-05 ), #4411, 'distance_accuracy_value', 'NONE');
#515=CIRCLE ( 'NONE', #57891, 0.2500000000000002220 ) ;
#525=CARTESIAN_POINT ( 'NONE',  ( 6.418790567836331284, -2.882328613363594361, 0.02778322089669375133 ) ) ;
#581=SURFACE_STYLE_USAGE ( .BOTH. , #6263 ) ;
#799=EDGE_LOOP ( 'NONE', ( #22119, #68329, #5663, #61545 ) ) ;
#978=CIRCLE ( 'NONE', #69598, 3.000000000000000444 ) ;
#1021=DIRECTION ( 'NONE',  ( -0.000000000000000000, -0.000000000000000000, -1.000000000000000000 ) ) ;
#1120=ORIENTED_EDGE ( 'NONE', *, *, #30649, .T. ) ;
#1145=EDGE_CURVE ( 'NONE', #47531, #52271, #24448, .T. ) ;
#1331=CARTESIAN_POINT ( 'NONE',  ( 1.401671290772265266, 7.000000000000007105, 0.1093172352041303641 ) ) ;
#1533=PRODUCT_DEFINITION_CONTEXT ( 'detailed design', #65785, 'design' ) ;
#1553=VECTOR ( 'NONE', #47217, 1000.000000000000000 ) ;
#1727=CARTESIAN_POINT ( 'NONE',  ( -7.440601873764707719, -1.112499515747335854, 0.4948905776603325646 ) ) ;
#1801=DIRECTION ( 'NONE',  ( -1.000000000000000000, 0.000000000000000000, 0.000000000000000000 ) ) ;
#1814=DIRECTION ( 'NONE',  ( 1.000000000000000000, 0.000000000000000000, 0.000000000000000000 ) ) ;
#1982=FACE_OUTER_BOUND ( 'NONE', #67167, .T. ) ;
#2007=CARTESIAN_POINT ( 'NONE',  ( 4.041451884327376121, 7.000000000000007105, 1.082903768654759569 ) ) ;
#2380=CARTESIAN_POINT ( 'NONE',  ( 0.000000000000000000, 0.000000000000000000, 7.500000000000000000 ) ) ;
#2389=( NAMED_UNIT ( * ) PLANE_ANGLE_UNIT ( ) SI_UNIT ( $, .RADIAN. ) );
#2436=DIRECTION ( 'NONE',  ( -0.5000000000000003331, -0.8660254037844384856, 0.000000000000000000 ) ) ;
#2457=VECTOR ( 'NONE', #51480, 1000.000000000000000 ) ;
#2519=AXIS2_PLACEMENT_3D ( 'NONE', #62965, #6302, #5953 ) ;
#2532=CARTESIAN_POINT ( 'NONE',  ( 6.062177826491071286, -3.500000000000002220, 0.000000000000000000 ) ) ;
#2953=EDGE_CURVE ( 'NONE', #57008, #55963, #47675, .T. ) ;
#3288=EDGE_CURVE ( 'NONE', #36954, #6981, #29941, .T. ) ;
#3348=MANIFOLD_SOLID_BREP ( 'Fillet1', #25039 ) ;
#3772=AXIS2_PLACEMENT_3D ( 'NONE', #15498, #20759, #36964 ) ;
#3832=DIRECTION ( 'NONE',  ( 0.000000000000000000, 1.000000000000000000, 0.000000000000000000 ) ) ;
#4026=CARTESIAN_POINT ( 'NONE',  ( 6.759171781091401598, 2.292771058063876932, 0.1074872947962648290 ) ) ;
#4074=LINE ( 'NONE', #68475, #67379 ) ;
#4183=EDGE_CURVE ( 'NONE', #45247, #63225, #25249, .T. ) ;
#4372=DIRECTION ( 'NONE',  ( -1.000000000000000000, 0.000000000000000000, 0.000000000000000000 ) ) ;
#4411=( LENGTH_UNIT ( ) NAMED_UNIT ( * ) SI_UNIT ( .MILLI., .METRE. ) );
#4581=CARTESIAN_POINT ( 'NONE',  ( 0.000000000000000000, 0.000000000000000000, 0.000000000000000000 ) ) ;
#4584=PLANE ( 'NONE',  #61168 ) ;
#4629=CIRCLE ( 'NONE', #24857, 7.000000000000001776 ) ;
#4872=CIRCLE ( 'NONE', #24004, 3.000000000000000444 ) ;
#4889=EDGE_LOOP ( 'NONE', ( #5242, #27167, #20305, #64424 ) ) ;
#4922=EDGE_CURVE ( 'NONE', #21587, #28936, #49364, .T. ) ;
#5136=ORIENTED_EDGE ( 'NONE', *, *, #63624, .T. ) ;
#5157=CARTESIAN_POINT ( 'NONE',  ( 0.000000000000000000, 0.000000000000000000, 1.000000000000000000 ) ) ;
#5242=ORIENTED_EDGE ( 'NONE', *, *, #30097, .T. ) ;
#5663=ORIENTED_EDGE ( 'NONE', *, *, #65850, .T. ) ;
#5720=DIRECTION ( 'NONE',  ( 0.000000000000000000, 0.000000000000000000, 1.000000000000000000 ) ) ;
#5849=CARTESIAN_POINT ( 'NONE',  ( 7.441974819423175624, -1.110121504110839430, 0.4967607073414704866 ) ) ;
#5855=DIRECTION ( 'NONE',  ( 0.8660254037844385966, -0.5000000000000001110, 0.000000000000000000 ) ) ;
#5953=DIRECTION ( 'NONE',  ( 1.000000000000000000, 0.000000000000000000, 0.000000000000000000 ) ) ;
#5971=ADVANCED_BREP_SHAPE_REPRESENTATION ( '', ( #3348, #42840 ), #43934 ) ;
#5979=DIRECTION ( 'NONE',  ( -0.7071067811865487940, 0.000000000000000000, 0.7071067811865463515 ) ) ;
#6019=FACE_OUTER_BOUND ( 'NONE', #56263, .T. ) ;
#6051=EDGE_CURVE ( 'NONE', #47531, #58312, #69080, .T. ) ;
#6080=CIRCLE ( 'NONE', #66742, 3.000000000000000444 ) ;
#6259=AXIS2_PLACEMENT_3D ( 'NONE', #9305, #52233, #52574 ) ;
#6263=SURFACE_SIDE_STYLE ('',( #65358 ) ) ;
#6302=DIRECTION ( 'NONE',  ( 0.000000000000000000, 0.000000000000000000, 1.000000000000000000 ) ) ;
#6319=B_SPLINE_CURVE_WITH_KNOTS ( 'NONE', 3,
 ( #11135, #54045, #5849, #27292, #48831, #525, #22053, #2532 ),
 .UNSPECIFIED., .F., .F.,
 ( 4, 2, 2, 4 ),
 ( 2.544316211736855218E-07, 0.002094919859796806443, 0.003142252573884622875, 0.004189585287972439308 ),
 .UNSPECIFIED. ) ;
#6320=ORIENTED_EDGE ( 'NONE', *, *, #56296, .F. ) ;
#6381=STYLED_ITEM ( 'NONE', ( #55434 ), #3348 ) ;
#6467=ORIENTED_EDGE ( 'NONE', *, *, #24963, .T. ) ;
#6653=ADVANCED_FACE ( 'NONE', ( #47536 ), #43183, .T. ) ;
#6700=DIRECTION ( 'NONE',  ( 1.000000000000000000, 0.000000000000000000, -0.000000000000000000 ) ) ;
#6769=CARTESIAN_POINT ( 'NONE',  ( 4.041451884327376121, 7.000000000000007105, 7.500000000000000000 ) ) ;
#6791=ORIENTED_EDGE ( 'NONE', *, *, #16162, .F. ) ;
#6981=VERTEX_POINT ( 'NONE', #42178 ) ;
#7217=DIRECTION ( 'NONE',  ( 0.000000000000000000, 0.000000000000000000, 1.000000000000000000 ) ) ;
#7352=ORIENTED_EDGE ( 'NONE', *, *, #9176, .F. ) ;
#7372=CARTESIAN_POINT ( 'NONE',  ( 3.728548500389067488, 7.000000000000006217, 0.9264520766856050304 ) ) ;
#7422=FACE_OUTER_BOUND ( 'NONE', #49574, .T. ) ;
#7553=EDGE_CURVE ( 'NONE', #16526, #22006, #6080, .T. ) ;
#7738=CARTESIAN_POINT ( 'NONE',  ( -6.759171781091402487, -2.292771058063873379, 0.1074872947962660502 ) ) ;
#7760=PLANE ( 'NONE',  #12918 ) ;
#7800=VECTOR ( 'NONE', #18508, 1000.000000000000000 ) ;
#7884=AXIS2_PLACEMENT_3D ( 'NONE', #10915, #31669, #53807 ) ;
#7885=CONICAL_SURFACE ( 'NONE', #31475, 7.000000000000000888, 0.7853981633974500554 ) ;
#8379=CARTESIAN_POINT ( 'NONE',  ( -3.414918479307655907, 7.000000000000006217, 0.7696370661449007944 ) ) ;
#8431=DIRECTION ( 'NONE',  ( -1.000000000000000000, 0.000000000000000000, 0.000000000000000000 ) ) ;
#8443=CARTESIAN_POINT ( 'NONE',  ( 3.000000000000000444, 3.673940397442060361E-16, 7.500000000000000000 ) ) ;
#8454=ORIENTED_EDGE ( 'NONE', *, *, #36279, .T. ) ;
#8513=CARTESIAN_POINT ( 'NONE',  ( 3.000000000000000444, 3.673940397442060361E-16, 32.50000000000000000 ) ) ;
#8576=EDGE_LOOP ( 'NONE', ( #56182, #68047 ) ) ;
#8577=CONICAL_SURFACE ( 'NONE', #27612, 7.000000000000000888, 0.7853981633974500554 ) ;
#8618=CARTESIAN_POINT ( 'NONE',  ( -5.249999999999997335, 0.000000000000000000, 0.000000000000000000 ) ) ;
#8681=DIRECTION ( 'NONE',  ( -0.5000000000000001110, -0.8660254037844385966, 0.000000000000000000 ) ) ;
#8743=LINE ( 'NONE', #14022, #35051 ) ;
#8764=CARTESIAN_POINT ( 'NONE',  ( 0.000000000000000000, 0.000000000000000000, 0.000000000000000000 ) ) ;
#9063=ORIENTED_EDGE ( 'NONE', *, *, #62794, .F. ) ;
#9105=ORIENTED_EDGE ( 'NONE', *, *, #6051, .T. ) ;
#9176=EDGE_CURVE ( 'NONE', #22804, #57008, #30412, .T. ) ;
#9305=CARTESIAN_POINT ( 'NONE',  ( 0.000000000000000000, 0.000000000000000000, 0.000000000000000000 ) ) ;
#9398=FILL_AREA_STYLE_COLOUR ( '', #33743 ) ;
#9421=EDGE_LOOP ( 'NONE', ( #7352, #45612, #9063, #68113, #16032 ) ) ;
#9561=CARTESIAN_POINT ( 'NONE',  ( 0.000000000000000000, 0.000000000000000000, 0.000000000000000000 ) ) ;
#9630=CARTESIAN_POINT ( 'NONE',  ( -2.755190520427473366, -7.000000000000002665, 0.4949495880430740402 ) ) ;
#9756=CARTESIAN_POINT ( 'NONE',  ( 0.000000000000000000, 0.000000000000000000, 0.2500000000000011102 ) ) ;
#9827=CARTESIAN_POINT ( 'NONE',  ( 0.000000000000000000, -7.000000000000000888, 0.000000000000000000 ) ) ;
#9879=ADVANCED_FACE ( 'NONE', ( #6019 ), #55597, .F. ) ;
#9881=ADVANCED_FACE ( 'NONE', ( #7422 ), #33448, .T. ) ;
#9882=CARTESIAN_POINT ( 'NONE',  ( -5.185928986913077132, -5.017707510222358280, 0.2088670156639313991 ) ) ;
#9920=CARTESIAN_POINT ( 'NONE',  ( 0.000000000000000000, 0.000000000000000000, 0.000000000000000000 ) ) ;
#9929=VERTEX_POINT ( 'NONE', #28131 ) ;
#9966=CARTESIAN_POINT ( 'NONE',  ( -1.403516486455608892, -7.000000000000002665, 0.1310752030855618366 ) ) ;
#9984=ADVANCED_FACE ( 'NONE', ( #24965 ), #35877, .F. ) ;
#10112=EDGE_CURVE ( 'NONE', #9929, #58002, #56278, .T. ) ;
#10148=ORIENTED_EDGE ( 'NONE', *, *, #1145, .F. ) ;
#10171=FILL_AREA_STYLE ('',( #48184 ) ) ;
#10200=ADVANCED_FACE ( 'NONE', ( #15828 ), #14781, .F. ) ;
#10298=CIRCLE ( 'NONE', #29392, 3.000000000000000444 ) ;
#10573=VECTOR ( 'NONE', #44603, 1000.000000000000114 ) ;
#10597=EDGE_LOOP ( 'NONE', ( #54410, #11323, #43655 ) ) ;
#10846=CARTESIAN_POINT ( 'NONE',  ( 4.041451884327379673, -7.000000000000002665, 1.082903768654758903 ) ) ;
#10882=DIRECTION ( 'NONE',  ( 0.000000000000000000, 0.000000000000000000, 1.000000000000000000 ) ) ;
#10894=CARTESIAN_POINT ( 'NONE',  ( 4.683753779217433078, -5.887500484252664812, 0.4948905776603311213 ) ) ;
#10915=CARTESIAN_POINT ( 'NONE',  ( 0.000000000000000000, 0.000000000000000000, 0.7500000000000000000 ) ) ;
#11012=DIRECTION ( 'NONE',  ( -0.000000000000000000, -0.000000000000000000, -1.000000000000000000 ) ) ;
#11135=CARTESIAN_POINT ( 'NONE',  ( 8.082903768654762899, -1.269775441351268174E-15, 1.082903768654759125 ) ) ;
#11201=DIRECTION ( 'NONE',  ( 0.000000000000000000, 0.000000000000000000, 1.000000000000000000 ) ) ;
#11232=ORIENTED_EDGE ( 'NONE', *, *, #10112, .F. ) ;
#11323=ORIENTED_EDGE ( 'NONE', *, *, #46868, .T. ) ;
#11842=CARTESIAN_POINT ( 'NONE',  ( 0.000000000000000000, 0.000000000000000000, 0.000000000000000000 ) ) ;
#11990=DIRECTION ( 'NONE',  ( -1.000000000000000000, 0.000000000000000000, 0.000000000000000000 ) ) ;
#12200=CARTESIAN_POINT ( 'NONE',  ( 4.041451884327379673, -7.000000000000002665, 1.082903768654758903 ) ) ;
#12209=EDGE_CURVE ( 'NONE', #17689, #29817, #16234, .T. ) ;
#12260=EDGE_LOOP ( 'NONE', ( #26211, #31571, #44676, #27351, #30210 ) ) ;
#12274=SHAPE_REPRESENTATION ( '16. Bolt M6x25', ( #42840 ), #43934 ) ;
#12335=DIRECTION ( 'NONE',  ( -1.224646799147353207E-16, 1.000000000000000000, 0.000000000000000000 ) ) ;
#12362=AXIS2_PLACEMENT_3D ( 'NONE', #2380, #22527, #55571 ) ;
#12386=CARTESIAN_POINT ( 'NONE',  ( 0.000000000000000000, 0.000000000000000000, 0.2500000000000011102 ) ) ;
#12627=CARTESIAN_POINT ( 'NONE',  ( 0.7098900097155618205, 7.000000000000007105, -1.987393404142764886E-14 ) ) ;
#12631=DIRECTION ( 'NONE',  ( -0.000000000000000000, -0.000000000000000000, -1.000000000000000000 ) ) ;
#12647=PLANE ( 'NONE',  #12362 ) ;
#12684=ORIENTED_EDGE ( 'NONE', *, *, #7553, .T. ) ;
#12731=AXIS2_PLACEMENT_3D ( 'NONE', #17820, #5855, #64623 ) ;
#12750=EDGE_LOOP ( 'NONE', ( #16203, #48412, #34808, #31904, #59442 ) ) ;
#12866=SURFACE_STYLE_FILL_AREA ( #45271 ) ;
#12918=AXIS2_PLACEMENT_3D ( 'NONE', #29205, #18683, #2436 ) ;
#12931=ORIENTED_EDGE ( 'NONE', *, *, #10112, .T. ) ;
#12955=DIRECTION ( 'NONE',  ( 0.000000000000000000, 0.000000000000000000, -1.000000000000000000 ) ) ;
#12998=FACE_OUTER_BOUND ( 'NONE', #21088, .T. ) ;
#13006=SURFACE_SIDE_STYLE ('',( #14664 ) ) ;
#13205=ORIENTED_EDGE ( 'NONE', *, *, #20842, .F. ) ;
#13242=VECTOR ( 'NONE', #67756, 1000.000000000000000 ) ;
#13260=ORIENTED_EDGE ( 'NONE', *, *, #16162, .T. ) ;
#13272=CARTESIAN_POINT ( 'NONE',  ( -0.3545099074454313715, 7.000000000000007994, -2.047617446692545640E-14 ) ) ;
#13550=MECHANICAL_DESIGN_GEOMETRIC_PRESENTATION_REPRESENTATION('',(#26989),#59601);
#13723=DIRECTION ( 'NONE',  ( 0.5000000000000003331, 0.8660254037844384856, 0.000000000000000000 ) ) ;
#13814=VERTEX_POINT ( 'NONE', #12200 ) ;
#13900=DIRECTION ( 'NONE',  ( 0.000000000000000000, 0.000000000000000000, 1.000000000000000000 ) ) ;
#13949=CARTESIAN_POINT ( 'NONE',  ( -4.041451884327381450, 7.000000000000006217, 7.500000000000000000 ) ) ;
#14022=CARTESIAN_POINT ( 'NONE',  ( -8.082903768654762899, 3.516382302766490365E-15, 7.500000000000000000 ) ) ;
#14073=CARTESIAN_POINT ( 'NONE',  ( -6.062177826491072175, -3.499999999999998668, 0.000000000000000000 ) ) ;
#14087=CARTESIAN_POINT ( 'NONE',  ( -4.041451884327381450, 7.000000000000006217, 7.500000000000000000 ) ) ;
#14338=CARTESIAN_POINT ( 'NONE',  ( 0.000000000000000000, 0.000000000000000000, 32.50000000000000000 ) ) ;
#14447=DIRECTION ( 'NONE',  ( 0.000000000000000000, 0.000000000000000000, 1.000000000000000000 ) ) ;
#14516=ORIENTED_EDGE ( 'NONE', *, *, #9176, .T. ) ;
#14664=SURFACE_STYLE_FILL_AREA ( #36133 ) ;
#14753=DIRECTION ( 'NONE',  ( 1.000000000000000000, 0.000000000000000000, 0.000000000000000000 ) ) ;
#14781=PLANE ( 'NONE',  #27923 ) ;
#14830=DIRECTION ( 'NONE',  ( 0.000000000000000000, 0.000000000000000000, 1.000000000000000000 ) ) ;
#14949=CONICAL_SURFACE ( 'NONE', #43049, 7.000000000000000888, 0.7853981633974500554 ) ;
#15152=CARTESIAN_POINT ( 'NONE',  ( 8.082903768654762899, -1.105959442090949618E-15, 7.500000000000000000 ) ) ;
#15215=ORIENTED_EDGE ( 'NONE', *, *, #12209, .F. ) ;
#15355=DIRECTION ( 'NONE',  ( 1.073081856240828566E-16, -1.000000000000000000, 0.000000000000000000 ) ) ;
#15388=LINE ( 'NONE', #16075, #64059 ) ;
#15408=MECHANICAL_DESIGN_GEOMETRIC_PRESENTATION_REPRESENTATION('',(#6381),#18732);
#15443=DIRECTION ( 'NONE',  ( 0.000000000000000000, 0.000000000000000000, 1.000000000000000000 ) ) ;
#15498=CARTESIAN_POINT ( 'NONE',  ( 0.000000000000000000, 0.000000000000000000, 0.000000000000000000 ) ) ;
#15510=CARTESIAN_POINT ( 'NONE',  ( -6.767634268437469736, 2.278113600022081631, 0.1324414877861203599 ) ) ;
#15527=ADVANCED_FACE ( 'NONE', ( #19297 ), #7885, .T. ) ;
#15528=FACE_OUTER_BOUND ( 'NONE', #33584, .T. ) ;
#15584=DIRECTION ( 'NONE',  ( 0.000000000000000000, 0.000000000000000000, -1.000000000000000000 ) ) ;
#15656=ORIENTED_EDGE ( 'NONE', *, *, #55417, .F. ) ;
#15803=VERTEX_POINT ( 'NONE', #40353 ) ;
#15807=FACE_OUTER_BOUND ( 'NONE', #30927, .T. ) ;
#15828=FACE_OUTER_BOUND ( 'NONE', #9421, .T. ) ;
#15859=CARTESIAN_POINT ( 'NONE',  ( -4.041451884327381450, -7.000000000000002665, 1.082903768654759791 ) ) ;
#15955=CARTESIAN_POINT ( 'NONE',  ( -0.7098155475105565326, -7.000000000000003553, 0.02753250691854188317 ) ) ;
#16032=ORIENTED_EDGE ( 'NONE', *, *, #23654, .F. ) ;
#16075=CARTESIAN_POINT ( 'NONE',  ( -8.082903768654762899, 3.516382302766490365E-15, 7.500000000000000000 ) ) ;
#16105=ORIENTED_EDGE ( 'NONE', *, *, #18268, .F. ) ;
#16156=ADVANCED_FACE ( 'NONE', ( #19401 ), #62318, .F. ) ;
#16162=EDGE_CURVE ( 'NONE', #42594, #55407, #978, .T. ) ;
#16165=PRESENTATION_STYLE_ASSIGNMENT (( #58697 ) ) ;
#16185=CIRCLE ( 'NONE', #34125, 5.249999999999997335 ) ;
#16203=ORIENTED_EDGE ( 'NONE', *, *, #47302, .F. ) ;
#16234=LINE ( 'NONE', #45049, #29284 ) ;
#16308=CARTESIAN_POINT ( 'NONE',  ( 0.000000000000000000, -7.000000000000000888, 0.000000000000000000 ) ) ;
#16490=EDGE_CURVE ( 'NONE', #58312, #47531, #21389, .T. ) ;
#16492=DIRECTION ( 'NONE',  ( 1.000000000000000000, 0.000000000000000000, 0.000000000000000000 ) ) ;
#16516=FILL_AREA_STYLE_COLOUR ( '', #35064 ) ;
#16526=VERTEX_POINT ( 'NONE', #8443 ) ;
#16537=ORIENTED_EDGE ( 'NONE', *, *, #35025, .T. ) ;
#16600=DIRECTION ( 'NONE',  ( 0.000000000000000000, 0.000000000000000000, -1.000000000000000000 ) ) ;
#16662=CONICAL_SURFACE ( 'NONE', #22253, 7.000000000000000888, 0.7853981633974500554 ) ;
#16677=DIRECTION ( 'NONE',  ( 0.000000000000000000, 0.000000000000000000, -1.000000000000000000 ) ) ;
#16695=EDGE_LOOP ( 'NONE', ( #45419, #41455, #27797 ) ) ;
#16973=EDGE_LOOP ( 'NONE', ( #50077, #19813, #34739, #45380 ) ) ;
#16987=CIRCLE ( 'NONE', #38343, 7.000000000000000888 ) ;
#17232=AXIS2_PLACEMENT_3D ( 'NONE', #14338, #57248, #51998 ) ;
#17652=ADVANCED_FACE ( 'NONE', ( #15807 ), #20230, .F. ) ;
#17663=FACE_OUTER_BOUND ( 'NONE', #23827, .T. ) ;
#17689=VERTEX_POINT ( 'NONE', #47922 ) ;
#17800=CARTESIAN_POINT ( 'NONE',  ( 0.000000000000000000, 0.000000000000000000, 1.000000000000000000 ) ) ;
#17820=CARTESIAN_POINT ( 'NONE',  ( -4.041451884327381450, 7.000000000000006217, 7.500000000000000000 ) ) ;
#17821=ORIENTED_EDGE ( 'NONE', *, *, #3288, .F. ) ;
#17870=CARTESIAN_POINT ( 'NONE',  ( 0.000000000000000000, 0.000000000000000000, 7.500000000000000000 ) ) ;
#17899=PLANE ( 'NONE',  #28899 ) ;
#17961=CARTESIAN_POINT ( 'NONE',  ( -7.766391886667110001, -0.5482146608018571010, 0.7663918866669822139 ) ) ;
#18268=EDGE_CURVE ( 'NONE', #28936, #63225, #27624, .T. ) ;
#18428=DIRECTION ( 'NONE',  ( 1.000000000000000000, 0.000000000000000000, 0.000000000000000000 ) ) ;
#18508=DIRECTION ( 'NONE',  ( -0.7071067811865426878, 0.000000000000000000, -0.7071067811865524577 ) ) ;
#18622=ORIENTED_EDGE ( 'NONE', *, *, #4922, .T. ) ;
#18683=DIRECTION ( 'NONE',  ( -0.8660254037844384856, 0.5000000000000003331, 0.000000000000000000 ) ) ;
#18704=ORIENTED_EDGE ( 'NONE', *, *, #51965, .T. ) ;
#18732=( GEOMETRIC_REPRESENTATION_CONTEXT ( 3 ) GLOBAL_UNCERTAINTY_ASSIGNED_CONTEXT ( ( #30409 ) ) GLOBAL_UNIT_ASSIGNED_CONTEXT ( ( #29378, #28684, #44924 ) ) REPRESENTATION_CONTEXT ( 'NONE', 'WORKASPACE' ) );
#18853=EDGE_CURVE ( 'NONE', #15803, #29817, #8743, .T. ) ;
#19155=AXIS2_PLACEMENT_3D ( 'NONE', #12386, #16677, #27522 ) ;
#19225=CIRCLE ( 'NONE', #31595, 7.000000000000001776 ) ;
#19297=FACE_OUTER_BOUND ( 'NONE', #10597, .T. ) ;
#19401=FACE_OUTER_BOUND ( 'NONE', #4889, .T. ) ;
#19618=FACE_OUTER_BOUND ( 'NONE', #799, .T. ) ;
#19688=ORIENTED_EDGE ( 'NONE', *, *, #27279, .T. ) ;
#19789=B_SPLINE_CURVE_WITH_KNOTS ( 'NONE', 3,
 ( #52269, #62769, #4026, #48051, #57516, #42091 ),
 .UNSPECIFIED., .F., .F.,
 ( 4, 2, 4 ),
 ( 0.004189585287972442777, 0.006269578072783818512, 0.008349570857595195114 ),
 .UNSPECIFIED. ) ;
#19813=ORIENTED_EDGE ( 'NONE', *, *, #58070, .T. ) ;
#19883=FACE_OUTER_BOUND ( 'NONE', #12260, .T. ) ;
#20230=TOROIDAL_SURFACE ( 'NONE', #7884, 4.750000000000000000, 0.2500000000000000000 ) ;
#20305=ORIENTED_EDGE ( 'NONE', *, *, #16490, .T. ) ;
#20409=CARTESIAN_POINT ( 'NONE',  ( -8.082903768654762899, 3.463586619550771876E-15, 1.082903768654759125 ) ) ;
#20473=CIRCLE ( 'NONE', #24933, 4.750000000000000000 ) ;
#20737=CARTESIAN_POINT ( 'NONE',  ( -3.000000000000000444, 0.000000000000000000, 7.500000000000000000 ) ) ;
#20759=DIRECTION ( 'NONE',  ( 0.000000000000000000, 0.000000000000000000, 1.000000000000000000 ) ) ;
#20778=CARTESIAN_POINT ( 'NONE',  ( -5.705565085145812176, -4.117671386636407860, 0.02778322089669425093 ) ) ;
#20842=EDGE_CURVE ( 'NONE', #30586, #50171, #29098, .T. ) ;
#21086=VECTOR ( 'NONE', #8681, 1000.000000000000114 ) ;
#21088=EDGE_LOOP ( 'NONE', ( #67722, #12931, #21491, #48543, #41082, #18704 ) ) ;
#21359=CARTESIAN_POINT ( 'NONE',  ( -3.000000000000000444, 0.000000000000000000, 32.50000000000000000 ) ) ;
#21364=CARTESIAN_POINT ( 'NONE',  ( 0.000000000000000000, 0.000000000000000000, 32.50000000000000000 ) ) ;
#21388=B_SPLINE_CURVE_WITH_KNOTS ( 'NONE', 3,
 ( #15859, #41921, #41553, #9882, #32006, #20778, #36984, #58394 ),
 .UNSPECIFIED., .F., .F.,
 ( 4, 2, 2, 4 ),
 ( 2.544316211732959925E-07, 0.002094919859796807744, 0.003142252573884623743, 0.004189585287972440175 ),
 .UNSPECIFIED. ) ;
#21389=CIRCLE ( 'NONE', #56234, 5.000000000000000000 ) ;
#21397=( LENGTH_UNIT ( ) NAMED_UNIT ( * ) SI_UNIT ( .MILLI., .METRE. ) );
#21398=FACE_OUTER_BOUND ( 'NONE', #16973, .T. ) ;
#21399=ORIENTED_EDGE ( 'NONE', *, *, #56296, .T. ) ;
#21480=CIRCLE ( 'NONE', #27077, 5.249999999999997335 ) ;
#21491=ORIENTED_EDGE ( 'NONE', *, *, #62794, .T. ) ;
#21518=PRODUCT ( '16. Bolt M6x25', '16. Bolt M6x25', '', ( #50150 ) ) ;
#21587=VERTEX_POINT ( 'NONE', #58446 ) ;
#21606=TOROIDAL_SURFACE ( 'NONE', #58664, 4.750000000000000000, 0.2500000000000000000 ) ;
#21690=EDGE_CURVE ( 'NONE', #30586, #55963, #16987, .T. ) ;
#22006=VERTEX_POINT ( 'NONE', #20737 ) ;
#22023=EDGE_CURVE ( 'NONE', #22006, #16526, #10298, .T. ) ;
#22036=ORIENTED_EDGE ( 'NONE', *, *, #36740, .T. ) ;
#22053=CARTESIAN_POINT ( 'NONE',  ( 6.239160159721276244, -3.193457606803200566, 4.616329562535936848E-16 ) ) ;
#22106=( LENGTH_UNIT ( ) NAMED_UNIT ( * ) SI_UNIT ( .MILLI., .METRE. ) );
#22119=ORIENTED_EDGE ( 'NONE', *, *, #66890, .F. ) ;
#22253=AXIS2_PLACEMENT_3D ( 'NONE', #30431, #62112, #40340 ) ;
#22322=DIRECTION ( 'NONE',  ( -0.000000000000000000, -0.000000000000000000, -1.000000000000000000 ) ) ;
#22373=AXIS2_PLACEMENT_3D ( 'NONE', #67395, #51229, #66348 ) ;
#22435=EDGE_CURVE ( 'NONE', #6981, #36954, #20473, .T. ) ;
#22527=DIRECTION ( 'NONE',  ( 0.000000000000000000, 0.000000000000000000, 1.000000000000000000 ) ) ;
#22755=DIRECTION ( 'NONE',  ( 0.000000000000000000, 0.000000000000000000, 1.000000000000000000 ) ) ;
#22763=ORIENTED_EDGE ( 'NONE', *, *, #4922, .F. ) ;
#22804=VERTEX_POINT ( 'NONE', #36958 ) ;
#22866=CARTESIAN_POINT ( 'NONE',  ( -4.041451884327381450, 7.000000000000006217, 7.500000000000000000 ) ) ;
#23110=LINE ( 'NONE', #33990, #10573 ) ;
#23303=B_SPLINE_CURVE_WITH_KNOTS ( 'NONE', 3,
 ( #63663, #37679, #59077, #10894, #32335, #27035 ),
 .UNSPECIFIED., .F., .F.,
 ( 4, 2, 4 ),
 ( 0.004189585287972439308, 0.006269578072783813308, 0.008349570857595188175 ),
 .UNSPECIFIED. ) ;
#23384=PLANE ( 'NONE',  #57450 ) ;
#23599=CARTESIAN_POINT ( 'NONE',  ( 8.082903768654762899, -1.105959442090949618E-15, 7.500000000000000000 ) ) ;
#23654=EDGE_CURVE ( 'NONE', #57008, #55641, #19789, .T. ) ;
#23735=SHAPE_DEFINITION_REPRESENTATION ( #68112, #12274 ) ;
#23827=EDGE_LOOP ( 'NONE', ( #45542, #46677, #11232, #28273, #15656 ) ) ;
#23942=CARTESIAN_POINT ( 'NONE',  ( 5.000000000000000000, 6.123233995736766282E-16, 1.000000000000000000 ) ) ;
#24004=AXIS2_PLACEMENT_3D ( 'NONE', #21364, #15443, #16492 ) ;
#24117=FILL_AREA_STYLE_COLOUR ( '', #31033 ) ;
#24178=ORIENTED_EDGE ( 'NONE', *, *, #21690, .F. ) ;
#24182=CARTESIAN_POINT ( 'NONE',  ( -4.041451884327381450, 7.000000000000006217, 1.082903768654761345 ) ) ;
#24291=ADVANCED_FACE ( 'NONE', ( #51907 ), #25159, .T. ) ;
#24320=ORIENTED_EDGE ( 'NONE', *, *, #44917, .F. ) ;
#24374=DIRECTION ( 'NONE',  ( 0.000000000000000000, 0.000000000000000000, 1.000000000000000000 ) ) ;
#24448=LINE ( 'NONE', #35386, #7800 ) ;
#24651=DIRECTION ( 'NONE',  ( -0.000000000000000000, -0.000000000000000000, -1.000000000000000000 ) ) ;
#24745=PRODUCT_DEFINITION_FORMATION_WITH_SPECIFIED_SOURCE ( 'ANY', '', #21518, .NOT_KNOWN. ) ;
#24781=DIRECTION ( 'NONE',  ( 0.000000000000000000, 0.000000000000000000, -1.000000000000000000 ) ) ;
#24818=LINE ( 'NONE', #46335, #13242 ) ;
#24857=AXIS2_PLACEMENT_3D ( 'NONE', #53919, #5720, #27166 ) ;
#24933=AXIS2_PLACEMENT_3D ( 'NONE', #17800, #24781, #46298 ) ;
#24963=EDGE_CURVE ( 'NONE', #30586, #17689, #43055, .T. ) ;
#24965=FACE_OUTER_BOUND ( 'NONE', #39289, .T. ) ;
#25010=DIRECTION ( 'NONE',  ( -1.000000000000000000, 0.000000000000000000, 0.000000000000000000 ) ) ;
#25039=CLOSED_SHELL ( 'NONE', ( #60689, #60835, #16156, #25973, #24291, #9984, #58022, #10200, #37057, #55802, #52944, #44702, #46696, #9881, #15527, #42393, #39605, #55918, #6653, #66000, #63293, #9879, #58451, #53450, #17652 ) ) ;
#25096=CARTESIAN_POINT ( 'NONE',  ( 0.000000000000000000, 0.000000000000000000, 0.000000000000000000 ) ) ;
#25159=CYLINDRICAL_SURFACE ( 'NONE', #67604, 3.000000000000000444 ) ;
#25249=LINE ( 'NONE', #57614, #40284 ) ;
#25351=ORIENTED_EDGE ( 'NONE', *, *, #12209, .T. ) ;
#25540=VECTOR ( 'NONE', #48149, 1000.000000000000000 ) ;
#25696=LINE ( 'NONE', #29328, #1553 ) ;
#25705=DIRECTION ( 'NONE',  ( -1.000000000000000000, 0.000000000000000000, 0.000000000000000000 ) ) ;
#25911=VECTOR ( 'NONE', #11012, 1000.000000000000000 ) ;
#25973=ADVANCED_FACE ( 'NONE', ( #15528 ), #14949, .T. ) ;
#26191=ORIENTED_EDGE ( 'NONE', *, *, #32554, .T. ) ;
#26211=ORIENTED_EDGE ( 'NONE', *, *, #39911, .F. ) ;
#26577=EDGE_CURVE ( 'NONE', #55407, #42594, #4872, .T. ) ;
#26758=ORIENTED_EDGE ( 'NONE', *, *, #27279, .F. ) ;
#26987=UNCERTAINTY_MEASURE_WITH_UNIT (LENGTH_MEASURE( 1.000000000000000082E-05 ), #22106, 'distance_accuracy_value', 'NONE');
#26989=STYLED_ITEM ( 'NONE', ( #66478 ), #5971 ) ;
#26998=SURFACE_SIDE_STYLE ('',( #37290 ) ) ;
#27035=CARTESIAN_POINT ( 'NONE',  ( 4.041451884327379673, -7.000000000000002665, 1.082903768654758903 ) ) ;
#27047=EDGE_LOOP ( 'NONE', ( #46452, #49485, #58406, #22763, #33432, #43622, #38900 ) ) ;
#27077=AXIS2_PLACEMENT_3D ( 'NONE', #45253, #13900, #40300 ) ;
#27166=DIRECTION ( 'NONE',  ( 1.000000000000000000, 0.000000000000000000, 0.000000000000000000 ) ) ;
#27167=ORIENTED_EDGE ( 'NONE', *, *, #40616, .T. ) ;
#27272=DIRECTION ( 'NONE',  ( 0.000000000000000000, 0.000000000000000000, -1.000000000000000000 ) ) ;
#27279=EDGE_CURVE ( 'NONE', #58312, #40048, #25696, .T. ) ;
#27292=CARTESIAN_POINT ( 'NONE',  ( 6.938426666069066329, -1.982292489777644828, 0.2088670156639322040 ) ) ;
#27330=VECTOR ( 'NONE', #66396, 1000.000000000000000 ) ;
#27351=ORIENTED_EDGE ( 'NONE', *, *, #60049, .T. ) ;
#27456=DIRECTION ( 'NONE',  ( -0.000000000000000000, -0.000000000000000000, -1.000000000000000000 ) ) ;
#27522=DIRECTION ( 'NONE',  ( -1.000000000000000000, 0.000000000000000000, 0.000000000000000000 ) ) ;
#27530=CIRCLE ( 'NONE', #6259, 7.000000000000001776 ) ;
#27606=DIRECTION ( 'NONE',  ( 0.8660254037844388186, 0.4999999999999998335, -0.000000000000000000 ) ) ;
#27612=AXIS2_PLACEMENT_3D ( 'NONE', #53769, #52431, #63979 ) ;
#27624=B_SPLINE_CURVE_WITH_KNOTS ( 'NONE', 3,
 ( #16308, #57805, #15955, #9966, #69058, #9630, #31385, #32426 ),
 .UNSPECIFIED., .F., .F.,
 ( 4, 2, 2, 4 ),
 ( 0.008439684080927939078, 0.009486163742497470339, 0.01053264340406700160, 0.01262560272720606412 ),
 .UNSPECIFIED. ) ;
#27692=( NAMED_UNIT ( * ) PLANE_ANGLE_UNIT ( ) SI_UNIT ( $, .RADIAN. ) );
#27781=DIRECTION ( 'NONE',  ( -1.000000000000000000, 0.000000000000000000, 0.000000000000000000 ) ) ;
#27797=ORIENTED_EDGE ( 'NONE', *, *, #60215, .T. ) ;
#27923=AXIS2_PLACEMENT_3D ( 'NONE', #15152, #37306, #36261 ) ;
#28060=DIRECTION ( 'NONE',  ( -1.000000000000000000, 0.000000000000000000, -0.000000000000000000 ) ) ;
#28089=COLOUR_RGB ( '', 0.31764706, 0.68627451, 0.89019608) ;
#28131=CARTESIAN_POINT ( 'NONE',  ( 4.041451884327379673, -7.000000000000002665, 7.500000000000000000 ) ) ;
#28273=ORIENTED_EDGE ( 'NONE', *, *, #65277, .T. ) ;
#28323=SURFACE_STYLE_USAGE ( .BOTH. , #65644 ) ;
#28512=CARTESIAN_POINT ( 'NONE',  ( -4.041451884327381450, 7.000000000000006217, 1.082903768654761345 ) ) ;
#28588=CARTESIAN_POINT ( 'NONE',  ( 0.000000000000000000, 0.000000000000000000, 0.2500000000000011102 ) ) ;
#28684=( NAMED_UNIT ( * ) PLANE_ANGLE_UNIT ( ) SI_UNIT ( $, .RADIAN. ) );
#28729=EDGE_CURVE ( 'NONE', #35530, #57014, #45883, .T. ) ;
#28899=AXIS2_PLACEMENT_3D ( 'NONE', #61147, #12955, #28060 ) ;
#28936=VERTEX_POINT ( 'NONE', #45485 ) ;
#29069=CONICAL_SURFACE ( 'NONE', #22373, 7.000000000000000888, 0.7853981633974500554 ) ;
#29098=B_SPLINE_CURVE_WITH_KNOTS ( 'NONE', 3,
 ( #39787, #66483, #55578, #50312, #61519, #56966 ),
 .UNSPECIFIED., .F., .F.,
 ( 4, 2, 4 ),
 ( 0.004189585287972434971, 0.006269578072783811573, 0.008349570857595188175 ),
 .UNSPECIFIED. ) ;
#29205=CARTESIAN_POINT ( 'NONE',  ( 4.041451884327379673, -7.000000000000002665, 7.500000000000000000 ) ) ;
#29284=VECTOR ( 'NONE', #5979, 1000.000000000000000 ) ;
#29328=CARTESIAN_POINT ( 'NONE',  ( 5.000000000000000000, 6.123233995736766282E-16, 0.2500000000000011102 ) ) ;
#29378=( LENGTH_UNIT ( ) NAMED_UNIT ( * ) SI_UNIT ( .MILLI., .METRE. ) );
#29392=AXIS2_PLACEMENT_3D ( 'NONE', #17870, #11201, #39015 ) ;
#29491=EDGE_LOOP ( 'NONE', ( #30931, #56206, #35863, #5136, #13205 ) ) ;
#29612=CARTESIAN_POINT ( 'NONE',  ( 0.000000000000000000, 0.000000000000000000, 32.50000000000000000 ) ) ;
#29817=VERTEX_POINT ( 'NONE', #60407 ) ;
#29818=APPLICATION_CONTEXT ( 'automotive_design' ) ;
#29941=CIRCLE ( 'NONE', #43459, 4.750000000000000000 ) ;
#30053=CARTESIAN_POINT ( 'NONE',  ( 4.682380833558962507, 5.889878495889167453, 0.4967607073414696539 ) ) ;
#30097=EDGE_CURVE ( 'NONE', #41190, #37694, #31923, .T. ) ;
#30138=AXIS2_PLACEMENT_3D ( 'NONE', #60502, #27456, #11990 ) ;
#30210=ORIENTED_EDGE ( 'NONE', *, *, #68145, .F. ) ;
#30409=UNCERTAINTY_MEASURE_WITH_UNIT (LENGTH_MEASURE( 1.000000000000000082E-05 ), #29378, 'distance_accuracy_value', 'NONE');
#30412=B_SPLINE_CURVE_WITH_KNOTS ( 'NONE', 3,
 ( #30745, #62750, #30053, #36439, #62425, #36053, #35357, #57496 ),
 .UNSPECIFIED., .F., .F.,
 ( 4, 2, 2, 4 ),
 ( 2.544316211733585141E-07, 0.002094919859796809478, 0.003142252573884625911, 0.004189585287972442777 ),
 .UNSPECIFIED. ) ;
#30431=CARTESIAN_POINT ( 'NONE',  ( 0.000000000000000000, 0.000000000000000000, 0.000000000000000000 ) ) ;
#30499=CYLINDRICAL_SURFACE ( 'NONE', #17232, 3.000000000000000444 ) ;
#30586=VERTEX_POINT ( 'NONE', #67180 ) ;
#30649=EDGE_CURVE ( 'NONE', #21587, #29817, #36937, .T. ) ;
#30745=CARTESIAN_POINT ( 'NONE',  ( 4.041451884327376121, 7.000000000000007105, 1.082903768654759569 ) ) ;
#30771=CARTESIAN_POINT ( 'NONE',  ( 0.000000000000000000, 0.000000000000000000, 32.50000000000000000 ) ) ;
#30927=EDGE_LOOP ( 'NONE', ( #66166, #17821, #47780, #6320 ) ) ;
#30931=ORIENTED_EDGE ( 'NONE', *, *, #36279, .F. ) ;
#30971=EDGE_CURVE ( 'NONE', #58002, #55641, #45340, .T. ) ;
#30994=CARTESIAN_POINT ( 'NONE',  ( 0.000000000000000000, 0.000000000000000000, 1.000000000000000000 ) ) ;
#31033=COLOUR_RGB ( '', 0.31764706, 0.68627451, 0.89019608) ;
#31126=PLANE ( 'NONE',  #44321 ) ;
#31385=CARTESIAN_POINT ( 'NONE',  ( -3.414918479307654575, -7.000000000000001776, 0.7696370661448970196 ) ) ;
#31475=AXIS2_PLACEMENT_3D ( 'NONE', #8764, #62218, #8431 ) ;
#31571=ORIENTED_EDGE ( 'NONE', *, *, #63624, .F. ) ;
#31595=AXIS2_PLACEMENT_3D ( 'NONE', #9920, #36692, #58436 ) ;
#31669=DIRECTION ( 'NONE',  ( 0.000000000000000000, 0.000000000000000000, -1.000000000000000000 ) ) ;
#31807=ORIENTED_EDGE ( 'NONE', *, *, #35025, .F. ) ;
#31904=ORIENTED_EDGE ( 'NONE', *, *, #18853, .T. ) ;
#31922=LINE ( 'NONE', #21359, #25540 ) ;
#31923=CIRCLE ( 'NONE', #42084, 5.000000000000000000 ) ;
#31949=CARTESIAN_POINT ( 'NONE',  ( 2.755511676787088415, -7.000000000000004441, 0.5168645644872222888 ) ) ;
#32006=CARTESIAN_POINT ( 'NONE',  ( -5.356721384544678166, -4.721886399977921478, 0.1324414877861183337 ) ) ;
#32220=DIRECTION ( 'NONE',  ( 0.4999999999999997780, -0.8660254037844387076, 0.000000000000000000 ) ) ;
#32290=CARTESIAN_POINT ( 'NONE',  ( 1.401671290772266598, -7.000000000000003553, 0.1093172352041265755 ) ) ;
#32316=FACE_OUTER_BOUND ( 'NONE', #34869, .T. ) ;
#32335=CARTESIAN_POINT ( 'NONE',  ( 4.357963766315031684, -6.451785339198144342, 0.7663918866669806595 ) ) ;
#32426=CARTESIAN_POINT ( 'NONE',  ( -4.041451884327381450, -7.000000000000002665, 1.082903768654759791 ) ) ;
#32554=EDGE_CURVE ( 'NONE', #17689, #21587, #27530, .T. ) ;
#32639=( NAMED_UNIT ( * ) PLANE_ANGLE_UNIT ( ) SI_UNIT ( $, .RADIAN. ) );
#33113=CARTESIAN_POINT ( 'NONE',  ( 0.000000000000000000, 0.000000000000000000, 32.50000000000000000 ) ) ;
#33432=ORIENTED_EDGE ( 'NONE', *, *, #32554, .F. ) ;
#33448=PLANE ( 'NONE',  #52639 ) ;
#33511=LINE ( 'NONE', #6769, #25911 ) ;
#33584=EDGE_LOOP ( 'NONE', ( #6467, #25351, #8454 ) ) ;
#33711=CARTESIAN_POINT ( 'NONE',  ( 5.000000000000000000, 6.123233995736766282E-16, 0.2500000000000011102 ) ) ;
#33743=COLOUR_RGB ( '', 0.31764706, 0.68627451, 0.89019608) ;
#33990=CARTESIAN_POINT ( 'NONE',  ( 8.082903768654762899, -1.105959442090949618E-15, 7.500000000000000000 ) ) ;
#34094=CARTESIAN_POINT ( 'NONE',  ( 2.755511676787084419, 7.000000000000007105, 0.5168645644872258416 ) ) ;
#34125=AXIS2_PLACEMENT_3D ( 'NONE', #11842, #22755, #60029 ) ;
#34132=CARTESIAN_POINT ( 'NONE',  ( -6.413663052920317575, -2.891209729714697030, 1.212104147520903391E-15 ) ) ;
#34136=ORIENTED_EDGE ( 'NONE', *, *, #40616, .F. ) ;
#34739=ORIENTED_EDGE ( 'NONE', *, *, #30097, .F. ) ;
#34808=ORIENTED_EDGE ( 'NONE', *, *, #51965, .F. ) ;
#34869=EDGE_LOOP ( 'NONE', ( #51042, #57950, #18622 ) ) ;
#35025=EDGE_CURVE ( 'NONE', #40048, #52271, #21480, .T. ) ;
#35051=VECTOR ( 'NONE', #35483, 1000.000000000000000 ) ;
#35064=COLOUR_RGB ( '', 0.08235294, 0.09019608, 0.10196078) ;
#35172=CARTESIAN_POINT ( 'NONE',  ( -8.082903768654762899, 3.463586619550771876E-15, 1.082903768654759125 ) ) ;
#35209=CARTESIAN_POINT ( 'NONE',  ( 6.062177826491071286, -3.500000000000002220, 0.000000000000000000 ) ) ;
#35357=CARTESIAN_POINT ( 'NONE',  ( 5.885195493260862776, 3.806542393196805651, -4.285986713106759716E-16 ) ) ;
#35386=CARTESIAN_POINT ( 'NONE',  ( -5.000000000000000000, 0.000000000000000000, 0.2500000000000011102 ) ) ;
#35483=DIRECTION ( 'NONE',  ( -0.000000000000000000, -0.000000000000000000, -1.000000000000000000 ) ) ;
#35530=VERTEX_POINT ( 'NONE', #55518 ) ;
#35791=CARTESIAN_POINT ( 'NONE',  ( 5.249999999999997335, 6.429395695523601195E-16, 0.000000000000000000 ) ) ;
#35863=ORIENTED_EDGE ( 'NONE', *, *, #67253, .F. ) ;
#35877=PLANE ( 'NONE',  #61623 ) ;
#36029=VERTEX_POINT ( 'NONE', #35209 ) ;
#36053=CARTESIAN_POINT ( 'NONE',  ( 5.705565085145811288, 4.117671386636414077, 0.02778322089669325520 ) ) ;
#36101=CARTESIAN_POINT ( 'NONE',  ( 3.000000000000000444, 3.673940397442060361E-16, 32.50000000000000000 ) ) ;
#36133=FILL_AREA_STYLE ('',( #9398 ) ) ;
#36142=CARTESIAN_POINT ( 'NONE',  ( 0.000000000000000000, 0.000000000000000000, 0.7500000000000000000 ) ) ;
#36261=DIRECTION ( 'NONE',  ( 0.5000000000000003331, -0.8660254037844383745, 0.000000000000000000 ) ) ;
#36279=EDGE_CURVE ( 'NONE', #29817, #30586, #49844, .T. ) ;
#36308=FACE_BOUND ( 'NONE', #65181, .T. ) ;
#36439=CARTESIAN_POINT ( 'NONE',  ( 5.185928986913072691, 5.017707510222363609, 0.2088670156639309550 ) ) ;
#36572=VECTOR ( 'NONE', #12631, 1000.000000000000000 ) ;
#36599=CARTESIAN_POINT ( 'NONE',  ( 2.418535808707046542, -7.000000000000002665, 0.3989014552058374741 ) ) ;
#36692=DIRECTION ( 'NONE',  ( 0.000000000000000000, 0.000000000000000000, 1.000000000000000000 ) ) ;
#36740=EDGE_CURVE ( 'NONE', #52271, #40048, #16185, .T. ) ;
#36809=CARTESIAN_POINT ( 'NONE',  ( -4.750000000000000000, 0.000000000000000000, 1.000000000000000000 ) ) ;
#36937=B_SPLINE_CURVE_WITH_KNOTS ( 'NONE', 3,
 ( #14073, #34132, #7738, #1727, #17961, #35172 ),
 .UNSPECIFIED., .F., .F.,
 ( 4, 2, 4 ),
 ( 0.004189585287972440175, 0.006269578072783814175, 0.008349570857595188175 ),
 .UNSPECIFIED. ) ;
#36954=VERTEX_POINT ( 'NONE', #36809 ) ;
#36958=CARTESIAN_POINT ( 'NONE',  ( 4.041451884327376121, 7.000000000000007105, 1.082903768654759569 ) ) ;
#36964=DIRECTION ( 'NONE',  ( -1.000000000000000000, 0.000000000000000000, 0.000000000000000000 ) ) ;
#36984=CARTESIAN_POINT ( 'NONE',  ( -5.885195493260865440, -3.806542393196800766, 1.022368767335940312E-15 ) ) ;
#37057=ADVANCED_FACE ( 'NONE', ( #19883 ), #31126, .F. ) ;
#37129=DIRECTION ( 'NONE',  ( -1.000000000000000000, 0.000000000000000000, 0.000000000000000000 ) ) ;
#37284=ORIENTED_EDGE ( 'NONE', *, *, #51797, .T. ) ;
#37290=SURFACE_STYLE_FILL_AREA ( #10171 ) ;
#37306=DIRECTION ( 'NONE',  ( -0.8660254037844384856, -0.5000000000000004441, 0.000000000000000000 ) ) ;
#37333=CARTESIAN_POINT ( 'NONE',  ( -6.239160159721279797, 3.193457606803199678, 3.307663659028042824E-15 ) ) ;
#37644=CARTESIAN_POINT ( 'NONE',  ( 0.000000000000000000, 0.000000000000000000, 0.7500000000000000000 ) ) ;
#37679=CARTESIAN_POINT ( 'NONE',  ( 5.710692600061826774, -4.108790270285303414, 4.269046054161672230E-16 ) ) ;
#37694=VERTEX_POINT ( 'NONE', #47 ) ;
#37928=EDGE_LOOP ( 'NONE', ( #15215, #26191, #1120 ) ) ;
#37932=VECTOR ( 'NONE', #1021, 1000.000000000000000 ) ;
#37984=PRESENTATION_STYLE_ASSIGNMENT (( #581 ) ) ;
#38192=LINE ( 'NONE', #48404, #63714 ) ;
#38250=ORIENTED_EDGE ( 'NONE', *, *, #26577, .T. ) ;
#38343=AXIS2_PLACEMENT_3D ( 'NONE', #45080, #16600, #27781 ) ;
#38437=ORIENTED_EDGE ( 'NONE', *, *, #1145, .T. ) ;
#38492=MECHANICAL_DESIGN_GEOMETRIC_PRESENTATION_REPRESENTATION('',(#40722),#44112);
#38749=FACE_BOUND ( 'NONE', #8576, .T. ) ;
#38774=AXIS2_PLACEMENT_3D ( 'NONE', #28588, #27272, #1814 ) ;
#38900=ORIENTED_EDGE ( 'NONE', *, *, #21690, .T. ) ;
#39015=DIRECTION ( 'NONE',  ( 1.000000000000000000, 0.000000000000000000, 0.000000000000000000 ) ) ;
#39071=CARTESIAN_POINT ( 'NONE',  ( 3.409623619629272184, 7.000000000000006217, 0.7804846576204730324 ) ) ;
#39132=CARTESIAN_POINT ( 'NONE',  ( 4.750000000000000000, 5.817072295949927426E-16, 0.7500000000000000000 ) ) ;
#39289=EDGE_LOOP ( 'NONE', ( #24320, #56726, #53309, #55145, #16105 ) ) ;
#39605=ADVANCED_FACE ( 'NONE', ( #32316 ), #8577, .T. ) ;
#39757=LINE ( 'NONE', #22866, #36572 ) ;
#39787=CARTESIAN_POINT ( 'NONE',  ( -6.062177826491071286, 3.500000000000000888, 0.000000000000000000 ) ) ;
#39819=LINE ( 'NONE', #23942, #37932 ) ;
#39911=EDGE_CURVE ( 'NONE', #50171, #55963, #68099, .T. ) ;
#40048=VERTEX_POINT ( 'NONE', #35791 ) ;
#40284=VECTOR ( 'NONE', #52002, 1000.000000000000000 ) ;
#40300=DIRECTION ( 'NONE',  ( 1.000000000000000000, 0.000000000000000000, 0.000000000000000000 ) ) ;
#40327=VECTOR ( 'NONE', #13723, 1000.000000000000114 ) ;
#40340=DIRECTION ( 'NONE',  ( -1.000000000000000000, 0.000000000000000000, 0.000000000000000000 ) ) ;
#40353=CARTESIAN_POINT ( 'NONE',  ( -8.082903768654762899, 3.516382302766490365E-15, 7.500000000000000000 ) ) ;
#40484=DIRECTION ( 'NONE',  ( 0.000000000000000000, -0.000000000000000000, 1.000000000000000000 ) ) ;
#40616=EDGE_CURVE ( 'NONE', #37694, #58312, #39819, .T. ) ;
#40699=FACE_OUTER_BOUND ( 'NONE', #45929, .T. ) ;
#40722=STYLED_ITEM ( 'NONE', ( #37984 ), #60689 ) ;
#40998=CIRCLE ( 'NONE', #63416, 5.000000000000000000 ) ;
#41080=DIRECTION ( 'NONE',  ( 0.000000000000000000, 0.000000000000000000, -1.000000000000000000 ) ) ;
#41082=ORIENTED_EDGE ( 'NONE', *, *, #67253, .T. ) ;
#41163=DIRECTION ( 'NONE',  ( 0.000000000000000000, 0.000000000000000000, -1.000000000000000000 ) ) ;
#41190=VERTEX_POINT ( 'NONE', #54477 ) ;
#41297=EDGE_LOOP ( 'NONE', ( #26758, #48307, #38437, #31807 ) ) ;
#41379=CARTESIAN_POINT ( 'NONE',  ( 0.000000000000000000, 0.000000000000000000, 0.000000000000000000 ) ) ;
#41382=CARTESIAN_POINT ( 'NONE',  ( 4.041451884327376121, 7.000000000000007105, 7.500000000000000000 ) ) ;
#41455=ORIENTED_EDGE ( 'NONE', *, *, #44917, .T. ) ;
#41539=ORIENTED_EDGE ( 'NONE', *, *, #2953, .T. ) ;
#41553=CARTESIAN_POINT ( 'NONE',  ( -4.682380833558966948, -5.889878495889163013, 0.4967607073414698760 ) ) ;
#41774=( NAMED_UNIT ( * ) PLANE_ANGLE_UNIT ( ) SI_UNIT ( $, .RADIAN. ) );
#41921=CARTESIAN_POINT ( 'NONE',  ( -4.358330484967983587, -6.451150163859152187, 0.7660251680141582087 ) ) ;
#41937=FACE_OUTER_BOUND ( 'NONE', #27047, .T. ) ;
#42084=AXIS2_PLACEMENT_3D ( 'NONE', #36142, #50073, #1801 ) ;
#42091=CARTESIAN_POINT ( 'NONE',  ( 8.082903768654762899, -1.269775441351268174E-15, 1.082903768654759125 ) ) ;
#42178=CARTESIAN_POINT ( 'NONE',  ( 4.750000000000000000, 5.970153145843347347E-16, 1.000000000000000000 ) ) ;
#42352=DIRECTION ( 'NONE',  ( -0.000000000000000000, -1.000000000000000000, -0.000000000000000000 ) ) ;
#42393=ADVANCED_FACE ( 'NONE', ( #45968 ), #29069, .T. ) ;
#42501=DIRECTION ( 'NONE',  ( -1.000000000000000000, 0.000000000000000000, 0.000000000000000000 ) ) ;
#42594=VERTEX_POINT ( 'NONE', #36101 ) ;
#42696=AXIS2_PLACEMENT_3D ( 'NONE', #30994, #52491, #25705 ) ;
#42789=FACE_OUTER_BOUND ( 'NONE', #37928, .T. ) ;
#42840=AXIS2_PLACEMENT_3D ( 'NONE', #59977, #7217, #49786 ) ;
#42942=DIRECTION ( 'NONE',  ( 1.000000000000000000, 0.000000000000000000, 0.000000000000000000 ) ) ;
#43006=PRODUCT_DEFINITION ( 'UNKNOWN', '', #24745, #1533 ) ;
#43049=AXIS2_PLACEMENT_3D ( 'NONE', #4581, #14447, #25010 ) ;
#43055=CIRCLE ( 'NONE', #2519, 7.000000000000001776 ) ;
#43063=CONICAL_SURFACE ( 'NONE', #47528, 5.000000000000000000, 0.7853981633974415066 ) ;
#43183=CONICAL_SURFACE ( 'NONE', #3772, 7.000000000000000888, 0.7853981633974500554 ) ;
#43272=( NAMED_UNIT ( * ) SI_UNIT ( $, .STERADIAN. ) SOLID_ANGLE_UNIT ( ) );
#43367=EDGE_LOOP ( 'NONE', ( #64758, #24178, #53702 ) ) ;
#43459=AXIS2_PLACEMENT_3D ( 'NONE', #5157, #58985, #42501 ) ;
#43622=ORIENTED_EDGE ( 'NONE', *, *, #24963, .F. ) ;
#43655=ORIENTED_EDGE ( 'NONE', *, *, #60110, .T. ) ;
#43860=ORIENTED_EDGE ( 'NONE', *, *, #3288, .T. ) ;
#43934=( GEOMETRIC_REPRESENTATION_CONTEXT ( 3 ) GLOBAL_UNCERTAINTY_ASSIGNED_CONTEXT ( ( #130 ) ) GLOBAL_UNIT_ASSIGNED_CONTEXT ( ( #4411, #2389, #57566 ) ) REPRESENTATION_CONTEXT ( 'NONE', 'WORKASPACE' ) );
#44112=( GEOMETRIC_REPRESENTATION_CONTEXT ( 3 ) GLOBAL_UNCERTAINTY_ASSIGNED_CONTEXT ( ( #26987 ) ) GLOBAL_UNIT_ASSIGNED_CONTEXT ( ( #22106, #27692, #64314 ) ) REPRESENTATION_CONTEXT ( 'NONE', 'WORKASPACE' ) );
#44138=ORIENTED_EDGE ( 'NONE', *, *, #65850, .F. ) ;
#44321=AXIS2_PLACEMENT_3D ( 'NONE', #41382, #15355, #52284 ) ;
#44603=DIRECTION ( 'NONE',  ( -0.5000000000000003331, 0.8660254037844383745, 0.000000000000000000 ) ) ;
#44676=ORIENTED_EDGE ( 'NONE', *, *, #28729, .F. ) ;
#44702=ADVANCED_FACE ( 'NONE', ( #38749, #12998 ), #12647, .T. ) ;
#44858=CARTESIAN_POINT ( 'NONE',  ( 4.041451884327376121, 7.000000000000007105, 7.500000000000000000 ) ) ;
#44917=EDGE_CURVE ( 'NONE', #13814, #28936, #56801, .T. ) ;
#44922=AXIS2_PLACEMENT_3D ( 'NONE', #25096, #46609, #57811 ) ;
#44924=( NAMED_UNIT ( * ) SI_UNIT ( $, .STERADIAN. ) SOLID_ANGLE_UNIT ( ) );
#45040=( GEOMETRIC_REPRESENTATION_CONTEXT ( 3 ) GLOBAL_UNCERTAINTY_ASSIGNED_CONTEXT ( ( #47512 ) ) GLOBAL_UNIT_ASSIGNED_CONTEXT ( ( #21397, #32639, #43272 ) ) REPRESENTATION_CONTEXT ( 'NONE', 'WORKASPACE' ) );
#45049=CARTESIAN_POINT ( 'NONE',  ( -7.000000000000000888, 0.000000000000000000, 0.000000000000000000 ) ) ;
#45065=( NAMED_UNIT ( * ) SI_UNIT ( $, .STERADIAN. ) SOLID_ANGLE_UNIT ( ) );
#45080=CARTESIAN_POINT ( 'NONE',  ( 0.000000000000000000, 0.000000000000000000, 0.000000000000000000 ) ) ;
#45247=VERTEX_POINT ( 'NONE', #54206 ) ;
#45253=CARTESIAN_POINT ( 'NONE',  ( 0.000000000000000000, 0.000000000000000000, 0.000000000000000000 ) ) ;
#45271=FILL_AREA_STYLE ('',( #24117 ) ) ;
#45332=DIRECTION ( 'NONE',  ( 0.000000000000000000, 0.000000000000000000, -1.000000000000000000 ) ) ;
#45340=LINE ( 'NONE', #55134, #27330 ) ;
#45380=ORIENTED_EDGE ( 'NONE', *, *, #55004, .F. ) ;
#45419=ORIENTED_EDGE ( 'NONE', *, *, #55417, .T. ) ;
#45485=CARTESIAN_POINT ( 'NONE',  ( 0.000000000000000000, -7.000000000000000888, 0.000000000000000000 ) ) ;
#45542=ORIENTED_EDGE ( 'NONE', *, *, #46868, .F. ) ;
#45612=ORIENTED_EDGE ( 'NONE', *, *, #60049, .F. ) ;
#45748=CARTESIAN_POINT ( 'NONE',  ( 0.000000000000000000, 0.000000000000000000, 0.2500000000000011102 ) ) ;
#45829=ORIENTED_EDGE ( 'NONE', *, *, #66890, .T. ) ;
#45883=LINE ( 'NONE', #44858, #2457 ) ;
#45929=EDGE_LOOP ( 'NONE', ( #14516, #41539, #68855 ) ) ;
#45968=FACE_OUTER_BOUND ( 'NONE', #16695, .T. ) ;
#46116=CARTESIAN_POINT ( 'NONE',  ( -4.041451884327381450, -7.000000000000002665, 7.500000000000000000 ) ) ;
#46298=DIRECTION ( 'NONE',  ( -1.000000000000000000, 0.000000000000000000, 0.000000000000000000 ) ) ;
#46335=CARTESIAN_POINT ( 'NONE',  ( -4.041451884327381450, -7.000000000000002665, 7.500000000000000000 ) ) ;
#46452=ORIENTED_EDGE ( 'NONE', *, *, #2953, .F. ) ;
#46609=DIRECTION ( 'NONE',  ( 0.000000000000000000, 0.000000000000000000, 1.000000000000000000 ) ) ;
#46673=DIRECTION ( 'NONE',  ( -1.000000000000000000, 0.000000000000000000, 0.000000000000000000 ) ) ;
#46677=ORIENTED_EDGE ( 'NONE', *, *, #30971, .F. ) ;
#46696=ADVANCED_FACE ( 'NONE', ( #19618 ), #30499, .T. ) ;
#46868=EDGE_CURVE ( 'NONE', #55641, #36029, #6319, .T. ) ;
#46882=DIRECTION ( 'NONE',  ( 1.000000000000000000, 0.000000000000000000, -0.000000000000000000 ) ) ;
#47217=DIRECTION ( 'NONE',  ( 0.7071067811865426878, 8.659560562354873694E-17, -0.7071067811865524577 ) ) ;
#47239=EDGE_LOOP ( 'NONE', ( #6791, #45829, #12684, #44138 ) ) ;
#47302=EDGE_CURVE ( 'NONE', #63225, #21587, #21388, .T. ) ;
#47403=B_SPLINE_CURVE_WITH_KNOTS ( 'NONE', 3,
 ( #55897, #12627, #1331, #50624, #34094, #39071, #7372, #2007 ),
 .UNSPECIFIED., .F., .F.,
 ( 4, 2, 2, 4 ),
 ( 0.01132179082380021552, 0.01341090848792873130, 0.01445546731999298833, 0.01550002615205724535 ),
 .UNSPECIFIED. ) ;
#47449=CONICAL_SURFACE ( 'NONE', #19155, 5.000000000000000000, 0.7853981633974415066 ) ;
#47512=UNCERTAINTY_MEASURE_WITH_UNIT (LENGTH_MEASURE( 1.000000000000000082E-05 ), #21397, 'distance_accuracy_value', 'NONE');
#47528=AXIS2_PLACEMENT_3D ( 'NONE', #9756, #41080, #62494 ) ;
#47531=VERTEX_POINT ( 'NONE', #55172 ) ;
#47536=FACE_OUTER_BOUND ( 'NONE', #43367, .T. ) ;
#47559=CIRCLE ( 'NONE', #48642, 0.2500000000000000000 ) ;
#47675=CIRCLE ( 'NONE', #56590, 7.000000000000001776 ) ;
#47780=ORIENTED_EDGE ( 'NONE', *, *, #55004, .T. ) ;
#47816=EDGE_LOOP ( 'NONE', ( #65449, #19688, #69276, #10148 ) ) ;
#47922=CARTESIAN_POINT ( 'NONE',  ( -7.000000000000002665, 0.000000000000000000, 0.000000000000000000 ) ) ;
#48051=CARTESIAN_POINT ( 'NONE',  ( 7.440601873764706831, 1.112499515747338741, 0.4948905776603317874 ) ) ;
#48149=DIRECTION ( 'NONE',  ( -0.000000000000000000, -0.000000000000000000, -1.000000000000000000 ) ) ;
#48184=FILL_AREA_STYLE_COLOUR ( '', #28089 ) ;
#48307=ORIENTED_EDGE ( 'NONE', *, *, #6051, .F. ) ;
#48404=CARTESIAN_POINT ( 'NONE',  ( 4.041451884327379673, -7.000000000000002665, 7.500000000000000000 ) ) ;
#48412=ORIENTED_EDGE ( 'NONE', *, *, #4183, .F. ) ;
#48518=CARTESIAN_POINT ( 'NONE',  ( 3.409623619629276625, -7.000000000000002665, 0.7804846576204699238 ) ) ;
#48543=ORIENTED_EDGE ( 'NONE', *, *, #28729, .T. ) ;
#48642=AXIS2_PLACEMENT_3D ( 'NONE', #52868, #42352, #15584 ) ;
#48788=CONICAL_SURFACE ( 'NONE', #61133, 7.000000000000000888, 0.7853981633974500554 ) ;
#48831=CARTESIAN_POINT ( 'NONE',  ( 6.767634268437467959, -2.278113600022081631, 0.1324414877861178896 ) ) ;
#48881=FILL_AREA_STYLE ('',( #16516 ) ) ;
#48908=CARTESIAN_POINT ( 'NONE',  ( 0.000000000000000000, 0.000000000000000000, 0.000000000000000000 ) ) ;
#49124=DIRECTION ( 'NONE',  ( -0.4999999999999997780, 0.8660254037844387076, 0.000000000000000000 ) ) ;
#49364=CIRCLE ( 'NONE', #44922, 7.000000000000001776 ) ;
#49451=FACE_OUTER_BOUND ( 'NONE', #12750, .T. ) ;
#49474=STYLED_ITEM ( 'NONE', ( #16165 ), #17652 ) ;
#49485=ORIENTED_EDGE ( 'NONE', *, *, #60110, .F. ) ;
#49574=EDGE_LOOP ( 'NONE', ( #38250, #13260 ) ) ;
#49786=DIRECTION ( 'NONE',  ( 1.000000000000000000, 0.000000000000000000, 0.000000000000000000 ) ) ;
#49844=B_SPLINE_CURVE_WITH_KNOTS ( 'NONE', 3,
 ( #20409, #68965, #63667, #58743, #15510, #64006, #37333, #55166 ),
 .UNSPECIFIED., .F., .F.,
 ( 4, 2, 2, 4 ),
 ( 2.544316211735830308E-07, 0.002094919859796804274, 0.003142252573884619406, 0.004189585287972434971 ),
 .UNSPECIFIED. ) ;
#50073=DIRECTION ( 'NONE',  ( -0.000000000000000000, -0.000000000000000000, 1.000000000000000000 ) ) ;
#50077=ORIENTED_EDGE ( 'NONE', *, *, #22435, .F. ) ;
#50150=PRODUCT_CONTEXT ( 'NONE', #29818, 'mechanical' ) ;
#50171=VERTEX_POINT ( 'NONE', #28512 ) ;
#50312=CARTESIAN_POINT ( 'NONE',  ( -4.683753779217435742, 5.887500484252664812, 0.4948905776603345075 ) ) ;
#50624=CARTESIAN_POINT ( 'NONE',  ( 2.418535808707042101, 7.000000000000006217, 0.3989014552058406382 ) ) ;
#51042=ORIENTED_EDGE ( 'NONE', *, *, #18268, .T. ) ;
#51087=DIRECTION ( 'NONE',  ( 0.000000000000000000, 0.000000000000000000, 1.000000000000000000 ) ) ;
#51229=DIRECTION ( 'NONE',  ( 0.000000000000000000, 0.000000000000000000, 1.000000000000000000 ) ) ;
#51480=DIRECTION ( 'NONE',  ( -1.000000000000000000, -1.073081856240828566E-16, 0.000000000000000000 ) ) ;
#51583=LINE ( 'NONE', #13949, #21086 ) ;
#51623=CARTESIAN_POINT ( 'NONE',  ( -1.744870598150812802, 7.000000000000005329, 0.2069669095365387901 ) ) ;
#51639=CARTESIAN_POINT ( 'NONE',  ( 8.082903768654762899, -1.269775441351268174E-15, 1.082903768654759125 ) ) ;
#51740=MECHANICAL_DESIGN_GEOMETRIC_PRESENTATION_REPRESENTATION('',(#49474),#45040);
#51797=EDGE_CURVE ( 'NONE', #41190, #47531, #4074, .T. ) ;
#51907=FACE_OUTER_BOUND ( 'NONE', #47239, .T. ) ;
#51965=EDGE_CURVE ( 'NONE', #15803, #45247, #15388, .T. ) ;
#51998=DIRECTION ( 'NONE',  ( -1.000000000000000000, 0.000000000000000000, 0.000000000000000000 ) ) ;
#52002=DIRECTION ( 'NONE',  ( -0.000000000000000000, -0.000000000000000000, -1.000000000000000000 ) ) ;
#52233=DIRECTION ( 'NONE',  ( 0.000000000000000000, 0.000000000000000000, 1.000000000000000000 ) ) ;
#52269=CARTESIAN_POINT ( 'NONE',  ( 6.062177826491070398, 3.500000000000002665, 0.000000000000000000 ) ) ;
#52271=VERTEX_POINT ( 'NONE', #8618 ) ;
#52272=DIRECTION ( 'NONE',  ( -0.000000000000000000, -0.000000000000000000, -1.000000000000000000 ) ) ;
#52284=DIRECTION ( 'NONE',  ( 1.000000000000000000, 1.073081856240828566E-16, 0.000000000000000000 ) ) ;
#52431=DIRECTION ( 'NONE',  ( 0.000000000000000000, 0.000000000000000000, 1.000000000000000000 ) ) ;
#52491=DIRECTION ( 'NONE',  ( -0.000000000000000000, -0.000000000000000000, -1.000000000000000000 ) ) ;
#52574=DIRECTION ( 'NONE',  ( 1.000000000000000000, 0.000000000000000000, 0.000000000000000000 ) ) ;
#52639=AXIS2_PLACEMENT_3D ( 'NONE', #33113, #59467, #6700 ) ;
#52868=CARTESIAN_POINT ( 'NONE',  ( -4.750000000000000000, 0.000000000000000000, 0.7500000000000000000 ) ) ;
#52944=ADVANCED_FACE ( 'NONE', ( #49451 ), #23384, .F. ) ;
#53309=ORIENTED_EDGE ( 'NONE', *, *, #66111, .F. ) ;
#53450=ADVANCED_FACE ( 'NONE', ( #60567 ), #47449, .F. ) ;
#53702=ORIENTED_EDGE ( 'NONE', *, *, #20842, .T. ) ;
#53740=CARTESIAN_POINT ( 'NONE',  ( 0.7098900097155632638, -7.000000000000000888, -2.373649839567916678E-14 ) ) ;
#53769=CARTESIAN_POINT ( 'NONE',  ( 0.000000000000000000, 0.000000000000000000, 0.000000000000000000 ) ) ;
#53807=DIRECTION ( 'NONE',  ( -1.000000000000000000, 0.000000000000000000, 0.000000000000000000 ) ) ;
#53919=CARTESIAN_POINT ( 'NONE',  ( 0.000000000000000000, 0.000000000000000000, 0.000000000000000000 ) ) ;
#54045=CARTESIAN_POINT ( 'NONE',  ( 7.766025168014160762, -0.5488498361408512549, 0.7660251680141582087 ) ) ;
#54049=FACE_OUTER_BOUND ( 'NONE', #29491, .T. ) ;
#54206=CARTESIAN_POINT ( 'NONE',  ( -4.041451884327381450, -7.000000000000002665, 7.500000000000000000 ) ) ;
#54410=ORIENTED_EDGE ( 'NONE', *, *, #23654, .T. ) ;
#54477=CARTESIAN_POINT ( 'NONE',  ( -5.000000000000000000, 0.000000000000000000, 0.7500000000000000000 ) ) ;
#55004=EDGE_CURVE ( 'NONE', #36954, #41190, #47559, .T. ) ;
#55037=CARTESIAN_POINT ( 'NONE',  ( -8.082903768654762899, 3.516382302766490365E-15, 7.500000000000000000 ) ) ;
#55134=CARTESIAN_POINT ( 'NONE',  ( 8.082903768654762899, -1.105959442090949618E-15, 7.500000000000000000 ) ) ;
#55145=ORIENTED_EDGE ( 'NONE', *, *, #4183, .T. ) ;
#55166=CARTESIAN_POINT ( 'NONE',  ( -6.062177826491071286, 3.500000000000000888, 0.000000000000000000 ) ) ;
#55172=CARTESIAN_POINT ( 'NONE',  ( -5.000000000000000000, 0.000000000000000000, 0.2500000000000011102 ) ) ;
#55407=VERTEX_POINT ( 'NONE', #68962 ) ;
#55417=EDGE_CURVE ( 'NONE', #36029, #13814, #23303, .T. ) ;
#55434=PRESENTATION_STYLE_ASSIGNMENT (( #28323 ) ) ;
#55518=CARTESIAN_POINT ( 'NONE',  ( 4.041451884327376121, 7.000000000000007105, 7.500000000000000000 ) ) ;
#55571=DIRECTION ( 'NONE',  ( 1.000000000000000000, 0.000000000000000000, -0.000000000000000000 ) ) ;
#55578=CARTESIAN_POINT ( 'NONE',  ( -5.365183871890746303, 4.707228941936129729, 0.1074872947962681735 ) ) ;
#55597=CYLINDRICAL_SURFACE ( 'NONE', #30138, 5.000000000000000000 ) ;
#55641=VERTEX_POINT ( 'NONE', #51639 ) ;
#55802=ADVANCED_FACE ( 'NONE', ( #54049 ), #65307, .F. ) ;
#55897=CARTESIAN_POINT ( 'NONE',  ( -7.511572993685801073E-16, 7.000000000000000888, 0.000000000000000000 ) ) ;
#55918=ADVANCED_FACE ( 'NONE', ( #42789 ), #48788, .T. ) ;
#55963=VERTEX_POINT ( 'NONE', #68798 ) ;
#56182=ORIENTED_EDGE ( 'NONE', *, *, #22023, .F. ) ;
#56184=CARTESIAN_POINT ( 'NONE',  ( -7.511572993685801073E-16, 7.000000000000000888, 0.000000000000000000 ) ) ;
#56206=ORIENTED_EDGE ( 'NONE', *, *, #18853, .F. ) ;
#56234=AXIS2_PLACEMENT_3D ( 'NONE', #45748, #41163, #14753 ) ;
#56263=EDGE_LOOP ( 'NONE', ( #34136, #21399, #37284, #9105 ) ) ;
#56278=LINE ( 'NONE', #61902, #40327 ) ;
#56296=EDGE_CURVE ( 'NONE', #37694, #41190, #40998, .T. ) ;
#56590=AXIS2_PLACEMENT_3D ( 'NONE', #48908, #10882, #42942 ) ;
#56686=CARTESIAN_POINT ( 'NONE',  ( -4.041451884327381450, -7.000000000000002665, 1.082903768654759791 ) ) ;
#56694=LINE ( 'NONE', #8513, #60538 ) ;
#56726=ORIENTED_EDGE ( 'NONE', *, *, #65277, .F. ) ;
#56801=B_SPLINE_CURVE_WITH_KNOTS ( 'NONE', 3,
 ( #10846, #58017, #48518, #31949, #36599, #32290, #53740, #9827 ),
 .UNSPECIFIED., .F., .F.,
 ( 4, 2, 2, 4 ),
 ( 0.004248627969284164696, 0.005296391997195108725, 0.006344156025106052754, 0.008439684080927939078 ),
 .UNSPECIFIED. ) ;
#56899=CARTESIAN_POINT ( 'NONE',  ( -0.7098155475105580869, 7.000000000000003553, 0.02753250691854559548 ) ) ;
#56966=CARTESIAN_POINT ( 'NONE',  ( -4.041451884327381450, 7.000000000000006217, 1.082903768654761345 ) ) ;
#57008=VERTEX_POINT ( 'NONE', #68247 ) ;
#57014=VERTEX_POINT ( 'NONE', #14087 ) ;
#57208=( LENGTH_UNIT ( ) NAMED_UNIT ( * ) SI_UNIT ( .MILLI., .METRE. ) );
#57248=DIRECTION ( 'NONE',  ( -0.000000000000000000, -0.000000000000000000, -1.000000000000000000 ) ) ;
#57450=AXIS2_PLACEMENT_3D ( 'NONE', #55037, #27606, #49124 ) ;
#57496=CARTESIAN_POINT ( 'NONE',  ( 6.062177826491070398, 3.500000000000002665, 0.000000000000000000 ) ) ;
#57516=CARTESIAN_POINT ( 'NONE',  ( 7.766391886667110889, 0.5482146608018589884, 0.7663918866669823249 ) ) ;
#57566=( NAMED_UNIT ( * ) SI_UNIT ( $, .STERADIAN. ) SOLID_ANGLE_UNIT ( ) );
#57614=CARTESIAN_POINT ( 'NONE',  ( -4.041451884327381450, -7.000000000000002665, 7.500000000000000000 ) ) ;
#57805=CARTESIAN_POINT ( 'NONE',  ( -0.3545099074454303167, -7.000000000000004441, -2.440407800158045118E-14 ) ) ;
#57811=DIRECTION ( 'NONE',  ( 1.000000000000000000, 0.000000000000000000, 0.000000000000000000 ) ) ;
#57891=AXIS2_PLACEMENT_3D ( 'NONE', #39132, #12335, #66157 ) ;
#57950=ORIENTED_EDGE ( 'NONE', *, *, #47302, .T. ) ;
#58002=VERTEX_POINT ( 'NONE', #23599 ) ;
#58017=CARTESIAN_POINT ( 'NONE',  ( 3.728548500389071485, -7.000000000000003553, 0.9264520766856032541 ) ) ;
#58022=ADVANCED_FACE ( 'NONE', ( #17663 ), #7760, .F. ) ;
#58070=EDGE_CURVE ( 'NONE', #6981, #37694, #515, .T. ) ;
#58312=VERTEX_POINT ( 'NONE', #33711 ) ;
#58394=CARTESIAN_POINT ( 'NONE',  ( -6.062177826491072175, -3.499999999999998668, 0.000000000000000000 ) ) ;
#58406=ORIENTED_EDGE ( 'NONE', *, *, #60215, .F. ) ;
#58436=DIRECTION ( 'NONE',  ( 1.000000000000000000, 0.000000000000000000, 0.000000000000000000 ) ) ;
#58446=CARTESIAN_POINT ( 'NONE',  ( -6.062177826491072175, -3.499999999999998668, 0.000000000000000000 ) ) ;
#58451=ADVANCED_FACE ( 'NONE', ( #1982 ), #17899, .T. ) ;
#58565=DIRECTION ( 'NONE',  ( 0.000000000000000000, 0.000000000000000000, 1.000000000000000000 ) ) ;
#58664=AXIS2_PLACEMENT_3D ( 'NONE', #37644, #45332, #66383 ) ;
#58697=SURFACE_STYLE_USAGE ( .BOTH. , #26998 ) ;
#58743=CARTESIAN_POINT ( 'NONE',  ( -6.938426666069068993, 1.982292489777645272, 0.2088670156639333142 ) ) ;
#58892=CARTESIAN_POINT ( 'NONE',  ( 0.000000000000000000, 0.000000000000000000, 0.7500000000000000000 ) ) ;
#58985=DIRECTION ( 'NONE',  ( 0.000000000000000000, 0.000000000000000000, -1.000000000000000000 ) ) ;
#59077=CARTESIAN_POINT ( 'NONE',  ( 5.365183871890743639, -4.707228941936128841, 0.1074872947962652175 ) ) ;
#59442=ORIENTED_EDGE ( 'NONE', *, *, #30649, .F. ) ;
#59467=DIRECTION ( 'NONE',  ( 0.000000000000000000, 0.000000000000000000, 1.000000000000000000 ) ) ;
#59561=DIRECTION ( 'NONE',  ( -0.000000000000000000, -0.000000000000000000, 1.000000000000000000 ) ) ;
#59601=( GEOMETRIC_REPRESENTATION_CONTEXT ( 3 ) GLOBAL_UNCERTAINTY_ASSIGNED_CONTEXT ( ( #65611 ) ) GLOBAL_UNIT_ASSIGNED_CONTEXT ( ( #57208, #41774, #45065 ) ) REPRESENTATION_CONTEXT ( 'NONE', 'WORKASPACE' ) );
#59977=CARTESIAN_POINT ( 'NONE',  ( 0.000000000000000000, 0.000000000000000000, 0.000000000000000000 ) ) ;
#60029=DIRECTION ( 'NONE',  ( 1.000000000000000000, 0.000000000000000000, 0.000000000000000000 ) ) ;
#60049=EDGE_CURVE ( 'NONE', #35530, #22804, #33511, .T. ) ;
#60110=EDGE_CURVE ( 'NONE', #36029, #57008, #4629, .T. ) ;
#60215=EDGE_CURVE ( 'NONE', #28936, #36029, #19225, .T. ) ;
#60407=CARTESIAN_POINT ( 'NONE',  ( -8.082903768654762899, 3.463586619550771876E-15, 1.082903768654759125 ) ) ;
#60502=CARTESIAN_POINT ( 'NONE',  ( 0.000000000000000000, 0.000000000000000000, 1.000000000000000000 ) ) ;
#60538=VECTOR ( 'NONE', #24651, 1000.000000000000000 ) ;
#60567=FACE_OUTER_BOUND ( 'NONE', #41297, .T. ) ;
#60689=ADVANCED_FACE ( 'NONE', ( #21398 ), #21606, .F. ) ;
#60835=ADVANCED_FACE ( 'NONE', ( #67426 ), #43063, .F. ) ;
#61133=AXIS2_PLACEMENT_3D ( 'NONE', #41379, #58565, #4372 ) ;
#61147=CARTESIAN_POINT ( 'NONE',  ( 0.000000000000000000, 0.000000000000000000, 1.000000000000000000 ) ) ;
#61168=AXIS2_PLACEMENT_3D ( 'NONE', #9561, #14830, #46882 ) ;
#61454=CARTESIAN_POINT ( 'NONE',  ( -1.403516486455610890, 7.000000000000006217, 0.1310752030855656391 ) ) ;
#61519=CARTESIAN_POINT ( 'NONE',  ( -4.357963766315036125, 6.451785339198147007, 0.7663918866669852115 ) ) ;
#61545=ORIENTED_EDGE ( 'NONE', *, *, #22023, .T. ) ;
#61623=AXIS2_PLACEMENT_3D ( 'NONE', #46116, #3832, #40484 ) ;
#61902=CARTESIAN_POINT ( 'NONE',  ( 4.041451884327379673, -7.000000000000002665, 7.500000000000000000 ) ) ;
#62112=DIRECTION ( 'NONE',  ( 0.000000000000000000, 0.000000000000000000, 1.000000000000000000 ) ) ;
#62218=DIRECTION ( 'NONE',  ( 0.000000000000000000, 0.000000000000000000, 1.000000000000000000 ) ) ;
#62318=CYLINDRICAL_SURFACE ( 'NONE', #42696, 5.000000000000000000 ) ;
#62425=CARTESIAN_POINT ( 'NONE',  ( 5.356721384544675502, 4.721886399977926807, 0.1324414877861175011 ) ) ;
#62486=SHAPE_REPRESENTATION_RELATIONSHIP ( 'NONE' , 'NONE' ,  #12274, #5971 ) ;
#62494=DIRECTION ( 'NONE',  ( -1.000000000000000000, 0.000000000000000000, 0.000000000000000000 ) ) ;
#62750=CARTESIAN_POINT ( 'NONE',  ( 4.358330484967979146, 6.451150163859158404, 0.7660251680141578756 ) ) ;
#62769=CARTESIAN_POINT ( 'NONE',  ( 6.413663052920311358, 2.891209729714700138, -4.192813088908785199E-16 ) ) ;
#62794=EDGE_CURVE ( 'NONE', #58002, #35530, #23110, .T. ) ;
#62965=CARTESIAN_POINT ( 'NONE',  ( 0.000000000000000000, 0.000000000000000000, 0.000000000000000000 ) ) ;
#63196=DIRECTION ( 'NONE',  ( -0.000000000000000000, -0.000000000000000000, -1.000000000000000000 ) ) ;
#63225=VERTEX_POINT ( 'NONE', #56686 ) ;
#63293=ADVANCED_FACE ( 'NONE', ( #36308, #41937 ), #4584, .F. ) ;
#63416=AXIS2_PLACEMENT_3D ( 'NONE', #58892, #59561, #37129 ) ;
#63624=EDGE_CURVE ( 'NONE', #57014, #50171, #39757, .T. ) ;
#63663=CARTESIAN_POINT ( 'NONE',  ( 6.062177826491071286, -3.500000000000002220, 0.000000000000000000 ) ) ;
#63667=CARTESIAN_POINT ( 'NONE',  ( -7.441974819423180065, 1.110121504110840762, 0.4967607073414712637 ) ) ;
#63714=VECTOR ( 'NONE', #22322, 1000.000000000000000 ) ;
#63979=DIRECTION ( 'NONE',  ( -1.000000000000000000, 0.000000000000000000, 0.000000000000000000 ) ) ;
#64006=CARTESIAN_POINT ( 'NONE',  ( -6.418790567836333949, 2.882328613363593917, 0.02778322089669647138 ) ) ;
#64059=VECTOR ( 'NONE', #32220, 1000.000000000000227 ) ;
#64314=( NAMED_UNIT ( * ) SI_UNIT ( $, .STERADIAN. ) SOLID_ANGLE_UNIT ( ) );
#64424=ORIENTED_EDGE ( 'NONE', *, *, #51797, .F. ) ;
#64623=DIRECTION ( 'NONE',  ( 0.5000000000000001110, 0.8660254037844385966, 0.000000000000000000 ) ) ;
#64758=ORIENTED_EDGE ( 'NONE', *, *, #39911, .T. ) ;
#65109=ORIENTED_EDGE ( 'NONE', *, *, #22435, .T. ) ;
#65181=EDGE_LOOP ( 'NONE', ( #22036, #16537 ) ) ;
#65277=EDGE_CURVE ( 'NONE', #9929, #13814, #38192, .T. ) ;
#65307=PLANE ( 'NONE',  #12731 ) ;
#65358=SURFACE_STYLE_FILL_AREA ( #48881 ) ;
#65449=ORIENTED_EDGE ( 'NONE', *, *, #16490, .F. ) ;
#65611=UNCERTAINTY_MEASURE_WITH_UNIT (LENGTH_MEASURE( 1.000000000000000082E-05 ), #57208, 'distance_accuracy_value', 'NONE');
#65644=SURFACE_SIDE_STYLE ('',( #12866 ) ) ;
#65785=APPLICATION_CONTEXT ( 'automotive_design' ) ;
#65850=EDGE_CURVE ( 'NONE', #55407, #22006, #31922, .T. ) ;
#66000=ADVANCED_FACE ( 'NONE', ( #40699 ), #16662, .T. ) ;
#66111=EDGE_CURVE ( 'NONE', #45247, #9929, #24818, .T. ) ;
#66157=DIRECTION ( 'NONE',  ( -1.000000000000000000, -1.224646799147353454E-16, 0.000000000000000000 ) ) ;
#66166=ORIENTED_EDGE ( 'NONE', *, *, #58070, .F. ) ;
#66348=DIRECTION ( 'NONE',  ( -1.000000000000000000, 0.000000000000000000, 0.000000000000000000 ) ) ;
#66383=DIRECTION ( 'NONE',  ( -1.000000000000000000, 0.000000000000000000, 0.000000000000000000 ) ) ;
#66396=DIRECTION ( 'NONE',  ( -0.000000000000000000, -0.000000000000000000, -1.000000000000000000 ) ) ;
#66478=PRESENTATION_STYLE_ASSIGNMENT (( #68831 ) ) ;
#66483=CARTESIAN_POINT ( 'NONE',  ( -5.710692600061829438, 4.108790270285304302, 3.163668057994810583E-15 ) ) ;
#66742=AXIS2_PLACEMENT_3D ( 'NONE', #67301, #24374, #18428 ) ;
#66890=EDGE_CURVE ( 'NONE', #42594, #16526, #56694, .T. ) ;
#67167=EDGE_LOOP ( 'NONE', ( #43860, #65109 ) ) ;
#67180=CARTESIAN_POINT ( 'NONE',  ( -6.062177826491071286, 3.500000000000000888, 0.000000000000000000 ) ) ;
#67248=DIRECTION ( 'NONE',  ( 1.000000000000000000, 0.000000000000000000, 0.000000000000000000 ) ) ;
#67253=EDGE_CURVE ( 'NONE', #57014, #15803, #51583, .T. ) ;
#67301=CARTESIAN_POINT ( 'NONE',  ( 0.000000000000000000, 0.000000000000000000, 7.500000000000000000 ) ) ;
#67379=VECTOR ( 'NONE', #63196, 1000.000000000000000 ) ;
#67395=CARTESIAN_POINT ( 'NONE',  ( 0.000000000000000000, 0.000000000000000000, 0.000000000000000000 ) ) ;
#67426=FACE_OUTER_BOUND ( 'NONE', #47816, .T. ) ;
#67604=AXIS2_PLACEMENT_3D ( 'NONE', #30771, #52272, #46673 ) ;
#67722=ORIENTED_EDGE ( 'NONE', *, *, #66111, .T. ) ;
#67756=DIRECTION ( 'NONE',  ( 1.000000000000000000, 0.000000000000000000, 0.000000000000000000 ) ) ;
#67805=CARTESIAN_POINT ( 'NONE',  ( -2.755190520427474699, 7.000000000000004441, 0.4949495880430779260 ) ) ;
#68047=ORIENTED_EDGE ( 'NONE', *, *, #7553, .F. ) ;
#68099=B_SPLINE_CURVE_WITH_KNOTS ( 'NONE', 3,
 ( #24182, #8379, #67805, #51623, #61454, #56899, #13272, #56184 ),
 .UNSPECIFIED., .F., .F.,
 ( 4, 2, 2, 4 ),
 ( 0.007148677244982143929, 0.009235234034391179292, 0.01027851242909569654, 0.01132179082380021552 ),
 .UNSPECIFIED. ) ;
#68112=PRODUCT_DEFINITION_SHAPE ( 'NONE', 'NONE',  #43006 ) ;
#68113=ORIENTED_EDGE ( 'NONE', *, *, #30971, .T. ) ;
#68145=EDGE_CURVE ( 'NONE', #55963, #22804, #47403, .T. ) ;
#68247=CARTESIAN_POINT ( 'NONE',  ( 6.062177826491070398, 3.500000000000002665, 0.000000000000000000 ) ) ;
#68329=ORIENTED_EDGE ( 'NONE', *, *, #26577, .F. ) ;
#68475=CARTESIAN_POINT ( 'NONE',  ( -5.000000000000000000, 0.000000000000000000, 1.000000000000000000 ) ) ;
#68798=CARTESIAN_POINT ( 'NONE',  ( -7.511572993685801073E-16, 7.000000000000000888, 0.000000000000000000 ) ) ;
#68831=SURFACE_STYLE_USAGE ( .BOTH. , #13006 ) ;
#68855=ORIENTED_EDGE ( 'NONE', *, *, #68145, .T. ) ;
#68962=CARTESIAN_POINT ( 'NONE',  ( -3.000000000000000444, 0.000000000000000000, 32.50000000000000000 ) ) ;
#68965=CARTESIAN_POINT ( 'NONE',  ( -7.766025168014158986, 0.5488498361408529203, 0.7660251680141585418 ) ) ;
#69058=CARTESIAN_POINT ( 'NONE',  ( -1.744870598150811469, -7.000000000000001776, 0.2069669095365348765 ) ) ;
#69080=CIRCLE ( 'NONE', #38774, 5.000000000000000000 ) ;
#69276=ORIENTED_EDGE ( 'NONE', *, *, #36740, .F. ) ;
#69598=AXIS2_PLACEMENT_3D ( 'NONE', #29612, #51087, #67248 ) ;
ENDSEC;
END-ISO-10303-21;
